ISO-10303-21;
HEADER;
/* Generated by software containing ST-Developer
 * from STEP Tools, Inc. (www.steptools.com) 
 */

FILE_DESCRIPTION(
/* description */ ('Jaw-coupled motor to shaft test stand'),
/* implementation_level */ '2;1');

FILE_NAME(
/* name */ 'Flat Washer - M8.step',
/* time_stamp */ '2026-10-27T10:46:06-07:00',
/* author */ (''),
/* organization */ (''),
/* preprocessor_version */ 'ST-DEVELOPER v20.2',
/* originating_system */ 'Autodesk Translation Framework v15.17.0.0',
/* authorisation */ '');

FILE_SCHEMA (('AUTOMOTIVE_DESIGN { 1 0 10303 214 3 1 1 }'));
ENDSEC;

DATA;
#10=MECHANICAL_DESIGN_GEOMETRIC_PRESENTATION_REPRESENTATION('',(#356),#19361);
#291=SHAPE_REPRESENTATION_RELATIONSHIP('SRR','None',#19506,#323);
#323=ADVANCED_BREP_SHAPE_REPRESENTATION('',(#389),#19342);
#356=STYLED_ITEM('',(#19753),#389);
#389=MANIFOLD_SOLID_BREP('Body1',#11000);
#479=FACE_BOUND('',#1886,.T.);
#480=FACE_BOUND('',#1888,.T.);
#628=PLANE('',#11667);
#629=PLANE('',#11668);
#1187=FACE_OUTER_BOUND('',#1883,.T.);
#1188=FACE_OUTER_BOUND('',#1884,.T.);
#1189=FACE_OUTER_BOUND('',#1885,.T.);
#1190=FACE_OUTER_BOUND('',#1887,.T.);
#1883=EDGE_LOOP('',(#8080,#8081,#8082,#8083));
#1884=EDGE_LOOP('',(#8084,#8085,#8086,#8087));
#1885=EDGE_LOOP('',(#8088));
#1886=EDGE_LOOP('',(#8089));
#1887=EDGE_LOOP('',(#8090));
#1888=EDGE_LOOP('',(#8091));
#2616=LINE('',#16644,#3769);
#2617=LINE('',#16650,#3770);
#3769=VECTOR('',#13161,0.42);
#3770=VECTOR('',#13168,0.8);
#4783=CIRCLE('',#11662,0.42);
#4784=CIRCLE('',#11663,0.42);
#4785=CIRCLE('',#11665,0.8);
#4786=CIRCLE('',#11666,0.8);
#5195=VERTEX_POINT('',#16641);
#5196=VERTEX_POINT('',#16643);
#5197=VERTEX_POINT('',#16647);
#5198=VERTEX_POINT('',#16649);
#6251=EDGE_CURVE('',#5195,#5195,#4783,.T.);
#6252=EDGE_CURVE('',#5195,#5196,#2616,.T.);
#6253=EDGE_CURVE('',#5196,#5196,#4784,.T.);
#6254=EDGE_CURVE('',#5197,#5197,#4785,.T.);
#6255=EDGE_CURVE('',#5197,#5198,#2617,.T.);
#6256=EDGE_CURVE('',#5198,#5198,#4786,.T.);
#8080=ORIENTED_EDGE('',*,*,#6251,.F.);
#8081=ORIENTED_EDGE('',*,*,#6252,.T.);
#8082=ORIENTED_EDGE('',*,*,#6253,.T.);
#8083=ORIENTED_EDGE('',*,*,#6252,.F.);
#8084=ORIENTED_EDGE('',*,*,#6254,.F.);
#8085=ORIENTED_EDGE('',*,*,#6255,.T.);
#8086=ORIENTED_EDGE('',*,*,#6256,.T.);
#8087=ORIENTED_EDGE('',*,*,#6255,.F.);
#8088=ORIENTED_EDGE('',*,*,#6254,.T.);
#8089=ORIENTED_EDGE('',*,*,#6251,.T.);
#8090=ORIENTED_EDGE('',*,*,#6256,.F.);
#8091=ORIENTED_EDGE('',*,*,#6253,.F.);
#10321=CYLINDRICAL_SURFACE('',#11661,0.42);
#10322=CYLINDRICAL_SURFACE('',#11664,0.8);
#10529=ADVANCED_FACE('',(#1187),#10321,.F.);
#10530=ADVANCED_FACE('',(#1188),#10322,.T.);
#10531=ADVANCED_FACE('',(#1189,#479),#628,.T.);
#10532=ADVANCED_FACE('',(#1190,#480),#629,.F.);
#11000=CLOSED_SHELL('',(#10529,#10530,#10531,#10532));
#11660=AXIS2_PLACEMENT_3D('',#16639,#13155,#13156);
#11661=AXIS2_PLACEMENT_3D('',#16640,#13157,#13158);
#11662=AXIS2_PLACEMENT_3D('',#16642,#13159,#13160);
#11663=AXIS2_PLACEMENT_3D('',#16645,#13162,#13163);
#11664=AXIS2_PLACEMENT_3D('',#16646,#13164,#13165);
#11665=AXIS2_PLACEMENT_3D('',#16648,#13166,#13167);
#11666=AXIS2_PLACEMENT_3D('',#16651,#13169,#13170);
#11667=AXIS2_PLACEMENT_3D('',#16652,#13171,#13172);
#11668=AXIS2_PLACEMENT_3D('',#16653,#13173,#13174);
#13155=DIRECTION('axis',(0.,0.,1.));
#13156=DIRECTION('refdir',(1.,0.,0.));
#13157=DIRECTION('center_axis',(0.,1.,0.));
#13158=DIRECTION('ref_axis',(1.,0.,0.));
#13159=DIRECTION('center_axis',(0.,-1.,0.));
#13160=DIRECTION('ref_axis',(1.,0.,0.));
#13161=DIRECTION('',(0.,-1.,0.));
#13162=DIRECTION('center_axis',(0.,-1.,0.));
#13163=DIRECTION('ref_axis',(1.,0.,0.));
#13164=DIRECTION('center_axis',(0.,1.,0.));
#13165=DIRECTION('ref_axis',(1.,0.,0.));
#13166=DIRECTION('center_axis',(0.,1.,0.));
#13167=DIRECTION('ref_axis',(1.,0.,0.));
#13168=DIRECTION('',(0.,-1.,0.));
#13169=DIRECTION('center_axis',(0.,1.,0.));
#13170=DIRECTION('ref_axis',(1.,0.,0.));
#13171=DIRECTION('center_axis',(0.,1.,0.));
#13172=DIRECTION('ref_axis',(1.,0.,0.));
#13173=DIRECTION('center_axis',(0.,1.,0.));
#13174=DIRECTION('ref_axis',(1.,0.,0.));
#16639=CARTESIAN_POINT('',(0.,0.,0.));
#16640=CARTESIAN_POINT('Origin',(0.,0.,0.));
#16641=CARTESIAN_POINT('',(-0.42,0.16,5.14351655641888E-17));
#16642=CARTESIAN_POINT('Origin',(0.,0.16,0.));
#16643=CARTESIAN_POINT('',(-0.42,0.,5.14351655641888E-17));
#16644=CARTESIAN_POINT('',(-0.42,0.,5.14351655641888E-17));
#16645=CARTESIAN_POINT('Origin',(0.,0.,0.));
#16646=CARTESIAN_POINT('Origin',(0.,0.,0.));
#16647=CARTESIAN_POINT('',(-0.8,0.16,9.79717439317883E-17));
#16648=CARTESIAN_POINT('Origin',(0.,0.16,0.));
#16649=CARTESIAN_POINT('',(-0.8,0.,9.79717439317883E-17));
#16650=CARTESIAN_POINT('',(-0.8,0.,9.79717439317883E-17));
#16651=CARTESIAN_POINT('Origin',(0.,0.,0.));
#16652=CARTESIAN_POINT('Origin',(0.,0.16,0.));
#16653=CARTESIAN_POINT('Origin',(0.,0.,0.));
#19304=UNCERTAINTY_MEASURE_WITH_UNIT(LENGTH_MEASURE(0.001),#19362,
'DISTANCE_ACCURACY_VALUE',
'Maximum model space distance between geometric entities at asserted c
onnectivities');
#19323=UNCERTAINTY_MEASURE_WITH_UNIT(LENGTH_MEASURE(0.001),#19362,
'DISTANCE_ACCURACY_VALUE',
'Maximum model space distance between geometric entities at asserted c
onnectivities');
#19342=(
GEOMETRIC_REPRESENTATION_CONTEXT(3)
GLOBAL_UNCERTAINTY_ASSIGNED_CONTEXT((#19304))
GLOBAL_UNIT_ASSIGNED_CONTEXT((#19362,#19364,#19365))
REPRESENTATION_CONTEXT('','3D')
);
#19361=(
GEOMETRIC_REPRESENTATION_CONTEXT(3)
GLOBAL_UNCERTAINTY_ASSIGNED_CONTEXT((#19323))
GLOBAL_UNIT_ASSIGNED_CONTEXT((#19362,#19364,#19365))
REPRESENTATION_CONTEXT('','3D')
);
#19362=(
LENGTH_UNIT()
NAMED_UNIT(*)
SI_UNIT(.CENTI.,.METRE.)
);
#19364=(
NAMED_UNIT(*)
PLANE_ANGLE_UNIT()
SI_UNIT($,.RADIAN.)
);
#19365=(
NAMED_UNIT(*)
SI_UNIT($,.STERADIAN.)
SOLID_ANGLE_UNIT()
);
#19384=SHAPE_DEFINITION_REPRESENTATION(#19423,#19506);
#19423=PRODUCT_DEFINITION_SHAPE('',$,#19544);
#19506=SHAPE_REPRESENTATION('',(#11660),#19342);
#19525=PRODUCT_DEFINITION_CONTEXT('part definition',#19638,'design');
#19544=PRODUCT_DEFINITION('Flat Washer - M8','Flat Washer - M8',#19581,
#19525);
#19581=PRODUCT_DEFINITION_FORMATION('',$,#19658);
#19638=APPLICATION_CONTEXT(
'Core Data for Automotive Mechanical Design Process');
#19639=PRODUCT_CONTEXT('part definition',#19638,'mechanical');
#19658=PRODUCT('Flat Washer - M8','Flat Washer - M8','Flat Washer - M8',
(#19639));
#19747=COLOUR_RGB('Black',0.12,0.14,0.17);
#19748=FILL_AREA_STYLE_COLOUR('',#19747);
#19749=FILL_AREA_STYLE('',(#19748));
#19750=SURFACE_STYLE_FILL_AREA(#19749);
#19751=SURFACE_SIDE_STYLE('',(#19750));
#19752=SURFACE_STYLE_USAGE(.BOTH.,#19751);
#19753=PRESENTATION_STYLE_ASSIGNMENT((#19752));
ENDSEC;
END-ISO-10303-21;
